ISO-10303-21;
HEADER;
/* Generated by software containing ST-Developer
 * from STEP Tools, Inc. (www.steptools.com) 
 */

FILE_DESCRIPTION(
/* description */ ('Twin-shaft manual slide'),
/* implementation_level */ '2;1');

FILE_NAME(
/* name */ 'Cap Screw - M5x20.step',
/* time_stamp */ '2026-10-27T18:38:08-07:00',
/* author */ (''),
/* organization */ (''),
/* preprocessor_version */ 'ST-DEVELOPER v20.2',
/* originating_system */ 'Autodesk Translation Framework v15.17.0.0',
/* authorisation */ '');

FILE_SCHEMA (('AUTOMOTIVE_DESIGN { 1 0 10303 214 3 1 1 }'));
ENDSEC;

DATA;
#10=MECHANICAL_DESIGN_GEOMETRIC_PRESENTATION_REPRESENTATION('',(#288),#6463);
#221=ORIENTED_CLOSED_SHELL('',*,#3653,.F.);
#225=BREP_WITH_VOIDS('Body1',#3652,(#221));
#236=CONICAL_SURFACE('',#4150,0.4,0.785398163397448);
#237=CONICAL_SURFACE('',#4154,0.41,0.785398163397448);
#238=CONICAL_SURFACE('',#4158,0.26,0.463647609000806);
#239=CONICAL_SURFACE('',#4162,0.225,0.785398163397448);
#256=SHAPE_REPRESENTATION_RELATIONSHIP('SRR','None',#6576,#272);
#272=ADVANCED_BREP_SHAPE_REPRESENTATION('',(#225),#6459);
#288=STYLED_ITEM('',(#6747),#225);
#395=FACE_BOUND('',#994,.T.);
#500=PLANE('',#4148);
#501=PLANE('',#4156);
#502=PLANE('',#4164);
#503=PLANE('',#4165);
#504=PLANE('',#4166);
#505=PLANE('',#4167);
#506=PLANE('',#4168);
#507=PLANE('',#4169);
#508=PLANE('',#4170);
#509=PLANE('',#4171);
#510=PLANE('',#4172);
#691=FACE_OUTER_BOUND('',#989,.T.);
#692=FACE_OUTER_BOUND('',#990,.T.);
#693=FACE_OUTER_BOUND('',#991,.T.);
#694=FACE_OUTER_BOUND('',#992,.T.);
#695=FACE_OUTER_BOUND('',#993,.T.);
#696=FACE_OUTER_BOUND('',#995,.T.);
#697=FACE_OUTER_BOUND('',#996,.T.);
#698=FACE_OUTER_BOUND('',#997,.T.);
#699=FACE_OUTER_BOUND('',#998,.T.);
#700=FACE_OUTER_BOUND('',#999,.T.);
#701=FACE_OUTER_BOUND('',#1000,.T.);
#702=FACE_OUTER_BOUND('',#1001,.T.);
#703=FACE_OUTER_BOUND('',#1002,.T.);
#704=FACE_OUTER_BOUND('',#1003,.T.);
#705=FACE_OUTER_BOUND('',#1004,.T.);
#706=FACE_OUTER_BOUND('',#1005,.T.);
#707=FACE_OUTER_BOUND('',#1006,.T.);
#989=EDGE_LOOP('',(#3214));
#990=EDGE_LOOP('',(#3215,#3216,#3217,#3218));
#991=EDGE_LOOP('',(#3219,#3220,#3221,#3222));
#992=EDGE_LOOP('',(#3223,#3224,#3225,#3226));
#993=EDGE_LOOP('',(#3227));
#994=EDGE_LOOP('',(#3228));
#995=EDGE_LOOP('',(#3229,#3230,#3231,#3232));
#996=EDGE_LOOP('',(#3233,#3234,#3235,#3236));
#997=EDGE_LOOP('',(#3237,#3238,#3239,#3240));
#998=EDGE_LOOP('',(#3241));
#999=EDGE_LOOP('',(#3242,#3243,#3244,#3245));
#1000=EDGE_LOOP('',(#3246,#3247,#3248,#3249));
#1001=EDGE_LOOP('',(#3250,#3251,#3252,#3253));
#1002=EDGE_LOOP('',(#3254,#3255,#3256,#3257));
#1003=EDGE_LOOP('',(#3258,#3259,#3260,#3261));
#1004=EDGE_LOOP('',(#3262,#3263,#3264,#3265));
#1005=EDGE_LOOP('',(#3266,#3267,#3268,#3269,#3270,#3271));
#1006=EDGE_LOOP('',(#3272,#3273,#3274,#3275,#3276,#3277));
#1271=LINE('',#6209,#1557);
#1272=LINE('',#6213,#1558);
#1273=LINE('',#6217,#1559);
#1274=LINE('',#6224,#1560);
#1275=LINE('',#6228,#1561);
#1276=LINE('',#6232,#1562);
#1277=LINE('',#6237,#1563);
#1278=LINE('',#6239,#1564);
#1279=LINE('',#6241,#1565);
#1280=LINE('',#6242,#1566);
#1281=LINE('',#6245,#1567);
#1282=LINE('',#6247,#1568);
#1283=LINE('',#6248,#1569);
#1284=LINE('',#6251,#1570);
#1285=LINE('',#6253,#1571);
#1286=LINE('',#6254,#1572);
#1287=LINE('',#6257,#1573);
#1288=LINE('',#6259,#1574);
#1289=LINE('',#6260,#1575);
#1290=LINE('',#6263,#1576);
#1291=LINE('',#6265,#1577);
#1292=LINE('',#6266,#1578);
#1293=LINE('',#6268,#1579);
#1294=LINE('',#6269,#1580);
#1557=VECTOR('',#5135,0.4);
#1558=VECTOR('',#5140,0.425);
#1559=VECTOR('',#5145,0.41);
#1560=VECTOR('',#5154,0.26);
#1561=VECTOR('',#5159,0.25);
#1562=VECTOR('',#5164,0.225);
#1563=VECTOR('',#5169,1.);
#1564=VECTOR('',#5170,1.);
#1565=VECTOR('',#5171,1.);
#1566=VECTOR('',#5172,1.);
#1567=VECTOR('',#5175,1.);
#1568=VECTOR('',#5176,1.);
#1569=VECTOR('',#5177,1.);
#1570=VECTOR('',#5180,1.);
#1571=VECTOR('',#5181,1.);
#1572=VECTOR('',#5182,1.);
#1573=VECTOR('',#5185,1.);
#1574=VECTOR('',#5186,1.);
#1575=VECTOR('',#5187,1.);
#1576=VECTOR('',#5190,1.);
#1577=VECTOR('',#5191,1.);
#1578=VECTOR('',#5192,1.);
#1579=VECTOR('',#5195,1.);
#1580=VECTOR('',#5196,1.);
#1738=CIRCLE('',#4149,0.375);
#1739=CIRCLE('',#4151,0.425);
#1740=CIRCLE('',#4153,0.425);
#1741=CIRCLE('',#4155,0.395);
#1742=CIRCLE('',#4157,0.27);
#1743=CIRCLE('',#4159,0.24505);
#1744=CIRCLE('',#4161,0.24505);
#1745=CIRCLE('',#4163,0.2);
#2001=VERTEX_POINT('',#6204);
#2002=VERTEX_POINT('',#6207);
#2003=VERTEX_POINT('',#6211);
#2004=VERTEX_POINT('',#6215);
#2005=VERTEX_POINT('',#6219);
#2006=VERTEX_POINT('',#6222);
#2007=VERTEX_POINT('',#6226);
#2008=VERTEX_POINT('',#6230);
#2009=VERTEX_POINT('',#6235);
#2010=VERTEX_POINT('',#6236);
#2011=VERTEX_POINT('',#6238);
#2012=VERTEX_POINT('',#6240);
#2013=VERTEX_POINT('',#6244);
#2014=VERTEX_POINT('',#6246);
#2015=VERTEX_POINT('',#6250);
#2016=VERTEX_POINT('',#6252);
#2017=VERTEX_POINT('',#6256);
#2018=VERTEX_POINT('',#6258);
#2019=VERTEX_POINT('',#6262);
#2020=VERTEX_POINT('',#6264);
#2412=EDGE_CURVE('',#2001,#2001,#1738,.T.);
#2413=EDGE_CURVE('',#2002,#2002,#1739,.T.);
#2414=EDGE_CURVE('',#2002,#2001,#1271,.T.);
#2415=EDGE_CURVE('',#2003,#2003,#1740,.T.);
#2416=EDGE_CURVE('',#2003,#2002,#1272,.T.);
#2417=EDGE_CURVE('',#2004,#2004,#1741,.T.);
#2418=EDGE_CURVE('',#2004,#2003,#1273,.T.);
#2419=EDGE_CURVE('',#2005,#2005,#1742,.T.);
#2420=EDGE_CURVE('',#2006,#2006,#1743,.F.);
#2421=EDGE_CURVE('',#2006,#2005,#1274,.T.);
#2422=EDGE_CURVE('',#2007,#2007,#1744,.F.);
#2423=EDGE_CURVE('',#2007,#2006,#1275,.T.);
#2424=EDGE_CURVE('',#2008,#2008,#1745,.T.);
#2425=EDGE_CURVE('',#2008,#2007,#1276,.T.);
#2426=EDGE_CURVE('',#2009,#2010,#1277,.T.);
#2427=EDGE_CURVE('',#2010,#2011,#1278,.T.);
#2428=EDGE_CURVE('',#2011,#2012,#1279,.T.);
#2429=EDGE_CURVE('',#2009,#2012,#1280,.T.);
#2430=EDGE_CURVE('',#2010,#2013,#1281,.T.);
#2431=EDGE_CURVE('',#2013,#2014,#1282,.T.);
#2432=EDGE_CURVE('',#2014,#2011,#1283,.T.);
#2433=EDGE_CURVE('',#2013,#2015,#1284,.T.);
#2434=EDGE_CURVE('',#2015,#2016,#1285,.T.);
#2435=EDGE_CURVE('',#2016,#2014,#1286,.T.);
#2436=EDGE_CURVE('',#2015,#2017,#1287,.T.);
#2437=EDGE_CURVE('',#2017,#2018,#1288,.T.);
#2438=EDGE_CURVE('',#2018,#2016,#1289,.T.);
#2439=EDGE_CURVE('',#2017,#2019,#1290,.T.);
#2440=EDGE_CURVE('',#2019,#2020,#1291,.T.);
#2441=EDGE_CURVE('',#2020,#2018,#1292,.T.);
#2442=EDGE_CURVE('',#2019,#2009,#1293,.T.);
#2443=EDGE_CURVE('',#2012,#2020,#1294,.T.);
#3214=ORIENTED_EDGE('',*,*,#2412,.F.);
#3215=ORIENTED_EDGE('',*,*,#2413,.F.);
#3216=ORIENTED_EDGE('',*,*,#2414,.T.);
#3217=ORIENTED_EDGE('',*,*,#2412,.T.);
#3218=ORIENTED_EDGE('',*,*,#2414,.F.);
#3219=ORIENTED_EDGE('',*,*,#2415,.F.);
#3220=ORIENTED_EDGE('',*,*,#2416,.T.);
#3221=ORIENTED_EDGE('',*,*,#2413,.T.);
#3222=ORIENTED_EDGE('',*,*,#2416,.F.);
#3223=ORIENTED_EDGE('',*,*,#2417,.F.);
#3224=ORIENTED_EDGE('',*,*,#2418,.T.);
#3225=ORIENTED_EDGE('',*,*,#2415,.T.);
#3226=ORIENTED_EDGE('',*,*,#2418,.F.);
#3227=ORIENTED_EDGE('',*,*,#2417,.T.);
#3228=ORIENTED_EDGE('',*,*,#2419,.F.);
#3229=ORIENTED_EDGE('',*,*,#2420,.F.);
#3230=ORIENTED_EDGE('',*,*,#2421,.T.);
#3231=ORIENTED_EDGE('',*,*,#2419,.T.);
#3232=ORIENTED_EDGE('',*,*,#2421,.F.);
#3233=ORIENTED_EDGE('',*,*,#2422,.F.);
#3234=ORIENTED_EDGE('',*,*,#2423,.T.);
#3235=ORIENTED_EDGE('',*,*,#2420,.T.);
#3236=ORIENTED_EDGE('',*,*,#2423,.F.);
#3237=ORIENTED_EDGE('',*,*,#2424,.F.);
#3238=ORIENTED_EDGE('',*,*,#2425,.T.);
#3239=ORIENTED_EDGE('',*,*,#2422,.T.);
#3240=ORIENTED_EDGE('',*,*,#2425,.F.);
#3241=ORIENTED_EDGE('',*,*,#2424,.T.);
#3242=ORIENTED_EDGE('',*,*,#2426,.T.);
#3243=ORIENTED_EDGE('',*,*,#2427,.T.);
#3244=ORIENTED_EDGE('',*,*,#2428,.T.);
#3245=ORIENTED_EDGE('',*,*,#2429,.F.);
#3246=ORIENTED_EDGE('',*,*,#2430,.T.);
#3247=ORIENTED_EDGE('',*,*,#2431,.T.);
#3248=ORIENTED_EDGE('',*,*,#2432,.T.);
#3249=ORIENTED_EDGE('',*,*,#2427,.F.);
#3250=ORIENTED_EDGE('',*,*,#2433,.T.);
#3251=ORIENTED_EDGE('',*,*,#2434,.T.);
#3252=ORIENTED_EDGE('',*,*,#2435,.T.);
#3253=ORIENTED_EDGE('',*,*,#2431,.F.);
#3254=ORIENTED_EDGE('',*,*,#2436,.T.);
#3255=ORIENTED_EDGE('',*,*,#2437,.T.);
#3256=ORIENTED_EDGE('',*,*,#2438,.T.);
#3257=ORIENTED_EDGE('',*,*,#2434,.F.);
#3258=ORIENTED_EDGE('',*,*,#2439,.T.);
#3259=ORIENTED_EDGE('',*,*,#2440,.T.);
#3260=ORIENTED_EDGE('',*,*,#2441,.T.);
#3261=ORIENTED_EDGE('',*,*,#2437,.F.);
#3262=ORIENTED_EDGE('',*,*,#2442,.T.);
#3263=ORIENTED_EDGE('',*,*,#2429,.T.);
#3264=ORIENTED_EDGE('',*,*,#2443,.T.);
#3265=ORIENTED_EDGE('',*,*,#2440,.F.);
#3266=ORIENTED_EDGE('',*,*,#2442,.F.);
#3267=ORIENTED_EDGE('',*,*,#2439,.F.);
#3268=ORIENTED_EDGE('',*,*,#2436,.F.);
#3269=ORIENTED_EDGE('',*,*,#2433,.F.);
#3270=ORIENTED_EDGE('',*,*,#2430,.F.);
#3271=ORIENTED_EDGE('',*,*,#2426,.F.);
#3272=ORIENTED_EDGE('',*,*,#2443,.F.);
#3273=ORIENTED_EDGE('',*,*,#2428,.F.);
#3274=ORIENTED_EDGE('',*,*,#2432,.F.);
#3275=ORIENTED_EDGE('',*,*,#2435,.F.);
#3276=ORIENTED_EDGE('',*,*,#2438,.F.);
#3277=ORIENTED_EDGE('',*,*,#2441,.F.);
#3423=CYLINDRICAL_SURFACE('',#4152,0.425);
#3424=CYLINDRICAL_SURFACE('',#4160,0.24505);
#3596=ADVANCED_FACE('',(#691),#500,.T.);
#3597=ADVANCED_FACE('',(#692),#236,.T.);
#3598=ADVANCED_FACE('',(#693),#3423,.T.);
#3599=ADVANCED_FACE('',(#694),#237,.T.);
#3600=ADVANCED_FACE('',(#695,#395),#501,.T.);
#3601=ADVANCED_FACE('',(#696),#238,.T.);
#3602=ADVANCED_FACE('',(#697),#3424,.T.);
#3603=ADVANCED_FACE('',(#698),#239,.T.);
#3604=ADVANCED_FACE('',(#699),#502,.T.);
#3605=ADVANCED_FACE('',(#700),#503,.F.);
#3606=ADVANCED_FACE('',(#701),#504,.F.);
#3607=ADVANCED_FACE('',(#702),#505,.F.);
#3608=ADVANCED_FACE('',(#703),#506,.F.);
#3609=ADVANCED_FACE('',(#704),#507,.F.);
#3610=ADVANCED_FACE('',(#705),#508,.F.);
#3611=ADVANCED_FACE('',(#706),#509,.F.);
#3612=ADVANCED_FACE('',(#707),#510,.F.);
#3652=CLOSED_SHELL('',(#3596,#3597,#3598,#3599,#3600,#3601,#3602,#3603,
#3604));
#3653=CLOSED_SHELL('',(#3605,#3606,#3607,#3608,#3609,#3610,#3611,#3612));
#4147=AXIS2_PLACEMENT_3D('',#6202,#5125,#5126);
#4148=AXIS2_PLACEMENT_3D('',#6203,#5127,#5128);
#4149=AXIS2_PLACEMENT_3D('',#6205,#5129,#5130);
#4150=AXIS2_PLACEMENT_3D('',#6206,#5131,#5132);
#4151=AXIS2_PLACEMENT_3D('',#6208,#5133,#5134);
#4152=AXIS2_PLACEMENT_3D('',#6210,#5136,#5137);
#4153=AXIS2_PLACEMENT_3D('',#6212,#5138,#5139);
#4154=AXIS2_PLACEMENT_3D('',#6214,#5141,#5142);
#4155=AXIS2_PLACEMENT_3D('',#6216,#5143,#5144);
#4156=AXIS2_PLACEMENT_3D('',#6218,#5146,#5147);
#4157=AXIS2_PLACEMENT_3D('',#6220,#5148,#5149);
#4158=AXIS2_PLACEMENT_3D('',#6221,#5150,#5151);
#4159=AXIS2_PLACEMENT_3D('',#6223,#5152,#5153);
#4160=AXIS2_PLACEMENT_3D('',#6225,#5155,#5156);
#4161=AXIS2_PLACEMENT_3D('',#6227,#5157,#5158);
#4162=AXIS2_PLACEMENT_3D('',#6229,#5160,#5161);
#4163=AXIS2_PLACEMENT_3D('',#6231,#5162,#5163);
#4164=AXIS2_PLACEMENT_3D('',#6233,#5165,#5166);
#4165=AXIS2_PLACEMENT_3D('',#6234,#5167,#5168);
#4166=AXIS2_PLACEMENT_3D('',#6243,#5173,#5174);
#4167=AXIS2_PLACEMENT_3D('',#6249,#5178,#5179);
#4168=AXIS2_PLACEMENT_3D('',#6255,#5183,#5184);
#4169=AXIS2_PLACEMENT_3D('',#6261,#5188,#5189);
#4170=AXIS2_PLACEMENT_3D('',#6267,#5193,#5194);
#4171=AXIS2_PLACEMENT_3D('',#6270,#5197,#5198);
#4172=AXIS2_PLACEMENT_3D('',#6271,#5199,#5200);
#5125=DIRECTION('axis',(0.,0.,1.));
#5126=DIRECTION('refdir',(1.,0.,0.));
#5127=DIRECTION('center_axis',(0.,1.,0.));
#5128=DIRECTION('ref_axis',(0.,0.,1.));
#5129=DIRECTION('center_axis',(0.,-1.,0.));
#5130=DIRECTION('ref_axis',(1.,0.,0.));
#5131=DIRECTION('center_axis',(0.,-1.,0.));
#5132=DIRECTION('ref_axis',(1.,0.,0.));
#5133=DIRECTION('center_axis',(0.,-1.,0.));
#5134=DIRECTION('ref_axis',(1.,0.,0.));
#5135=DIRECTION('',(0.707106781186548,0.707106781186547,8.65956056235493E-17));
#5136=DIRECTION('center_axis',(0.,-1.,0.));
#5137=DIRECTION('ref_axis',(1.,0.,0.));
#5138=DIRECTION('center_axis',(0.,-1.,0.));
#5139=DIRECTION('ref_axis',(1.,0.,0.));
#5140=DIRECTION('',(0.,1.,0.));
#5141=DIRECTION('center_axis',(0.,1.,0.));
#5142=DIRECTION('ref_axis',(1.,0.,0.));
#5143=DIRECTION('center_axis',(0.,-1.,0.));
#5144=DIRECTION('ref_axis',(1.,0.,0.));
#5145=DIRECTION('',(-0.707106781186547,0.707106781186548,-8.65956056235493E-17));
#5146=DIRECTION('center_axis',(0.,-1.,0.));
#5147=DIRECTION('ref_axis',(0.,0.,-1.));
#5148=DIRECTION('center_axis',(0.,-1.,0.));
#5149=DIRECTION('ref_axis',(1.,0.,0.));
#5150=DIRECTION('center_axis',(0.,1.,0.));
#5151=DIRECTION('ref_axis',(1.,0.,0.));
#5152=DIRECTION('center_axis',(0.,1.,0.));
#5153=DIRECTION('ref_axis',(1.,0.,0.));
#5154=DIRECTION('',(-0.447213595499958,0.894427190999916,-5.47678698264203E-17));
#5155=DIRECTION('center_axis',(0.,-1.,0.));
#5156=DIRECTION('ref_axis',(1.,0.,0.));
#5157=DIRECTION('center_axis',(0.,1.,0.));
#5158=DIRECTION('ref_axis',(1.,0.,0.));
#5159=DIRECTION('',(0.,1.,0.));
#5160=DIRECTION('center_axis',(0.,1.,0.));
#5161=DIRECTION('ref_axis',(1.,0.,0.));
#5162=DIRECTION('center_axis',(0.,-1.,0.));
#5163=DIRECTION('ref_axis',(1.,0.,0.));
#5164=DIRECTION('',(-0.707106781186547,0.707106781186548,-8.65956056235493E-17));
#5165=DIRECTION('center_axis',(0.,-1.,0.));
#5166=DIRECTION('ref_axis',(0.,0.,-1.));
#5167=DIRECTION('center_axis',(0.866025403784439,0.,-0.5));
#5168=DIRECTION('ref_axis',(0.5,0.,0.866025403784439));
#5169=DIRECTION('',(-0.5,0.,-0.866025403784439));
#5170=DIRECTION('',(0.,-1.,0.));
#5171=DIRECTION('',(0.5,0.,0.866025403784439));
#5172=DIRECTION('',(0.,-1.,0.));
#5173=DIRECTION('center_axis',(1.20185167898973E-16,0.,-1.));
#5174=DIRECTION('ref_axis',(1.,0.,1.20185167898973E-16));
#5175=DIRECTION('',(-1.,0.,-1.20185167898973E-16));
#5176=DIRECTION('',(0.,-1.,0.));
#5177=DIRECTION('',(1.,0.,1.20185167898973E-16));
#5178=DIRECTION('center_axis',(-0.866025403784439,0.,-0.5));
#5179=DIRECTION('ref_axis',(0.5,0.,-0.866025403784439));
#5180=DIRECTION('',(-0.5,0.,0.866025403784439));
#5181=DIRECTION('',(0.,-1.,0.));
#5182=DIRECTION('',(0.5,0.,-0.866025403784439));
#5183=DIRECTION('center_axis',(-0.866025403784439,0.,0.5));
#5184=DIRECTION('ref_axis',(-0.5,0.,-0.866025403784439));
#5185=DIRECTION('',(0.5,0.,0.866025403784439));
#5186=DIRECTION('',(0.,-1.,0.));
#5187=DIRECTION('',(-0.5,0.,-0.866025403784439));
#5188=DIRECTION('center_axis',(-2.40370335797945E-16,0.,1.));
#5189=DIRECTION('ref_axis',(-1.,0.,-2.40370335797945E-16));
#5190=DIRECTION('',(1.,0.,2.40370335797945E-16));
#5191=DIRECTION('',(0.,-1.,0.));
#5192=DIRECTION('',(-1.,0.,-2.40370335797945E-16));
#5193=DIRECTION('center_axis',(0.866025403784439,0.,0.5));
#5194=DIRECTION('ref_axis',(-0.5,0.,0.866025403784439));
#5195=DIRECTION('',(0.5,0.,-0.866025403784439));
#5196=DIRECTION('',(-0.5,0.,0.866025403784439));
#5197=DIRECTION('center_axis',(0.,1.,0.));
#5198=DIRECTION('ref_axis',(1.,0.,0.));
#5199=DIRECTION('center_axis',(0.,-1.,0.));
#5200=DIRECTION('ref_axis',(0.,0.,-1.));
#6202=CARTESIAN_POINT('',(0.,0.,0.));
#6203=CARTESIAN_POINT('Origin',(0.375,0.5,0.));
#6204=CARTESIAN_POINT('',(-0.375,0.5,-4.59242549680257E-17));
#6205=CARTESIAN_POINT('Origin',(0.,0.5,0.));
#6206=CARTESIAN_POINT('Origin',(0.,0.475,0.));
#6207=CARTESIAN_POINT('',(-0.425,0.45,-5.20474889637625E-17));
#6208=CARTESIAN_POINT('Origin',(0.,0.45,0.));
#6209=CARTESIAN_POINT('',(-0.4,0.475,-4.89858719658941E-17));
#6210=CARTESIAN_POINT('Origin',(0.,0.24,0.));
#6211=CARTESIAN_POINT('',(-0.425,0.0299999999999998,-5.20474889637625E-17));
#6212=CARTESIAN_POINT('Origin',(0.,0.0299999999999998,0.));
#6213=CARTESIAN_POINT('',(-0.425,0.24,-5.20474889637625E-17));
#6214=CARTESIAN_POINT('Origin',(0.,0.0150000000000001,0.));
#6215=CARTESIAN_POINT('',(-0.395,4.85722573273506E-17,-4.83735485663204E-17));
#6216=CARTESIAN_POINT('Origin',(0.,0.,0.));
#6217=CARTESIAN_POINT('',(-0.41,0.0150000000000001,-5.02105187650415E-17));
#6218=CARTESIAN_POINT('Origin',(0.27,0.,0.));
#6219=CARTESIAN_POINT('',(-0.27,0.,-3.30654635769785E-17));
#6220=CARTESIAN_POINT('Origin',(0.,0.,0.));
#6221=CARTESIAN_POINT('Origin',(0.,-0.02,0.));
#6222=CARTESIAN_POINT('',(-0.24505,-0.0498999999999999,3.00099698131059E-17));
#6223=CARTESIAN_POINT('Origin',(0.,-0.0498999999999999,0.));
#6224=CARTESIAN_POINT('',(-0.26,-0.02,-3.18408167778312E-17));
#6225=CARTESIAN_POINT('Origin',(0.,-0.995,0.));
#6226=CARTESIAN_POINT('',(-0.24505,-1.95495,3.00099698131059E-17));
#6227=CARTESIAN_POINT('Origin',(0.,-1.95495,0.));
#6228=CARTESIAN_POINT('',(-0.24505,-0.995,-3.00099698131059E-17));
#6229=CARTESIAN_POINT('Origin',(0.,-1.975,0.));
#6230=CARTESIAN_POINT('',(-0.2,-2.,-2.44929359829471E-17));
#6231=CARTESIAN_POINT('Origin',(0.,-2.,0.));
#6232=CARTESIAN_POINT('',(-0.225,-1.975,-2.75545529808154E-17));
#6233=CARTESIAN_POINT('Origin',(0.,-2.,0.));
#6234=CARTESIAN_POINT('Origin',(0.115470053837925,-0.5,-0.2));
#6235=CARTESIAN_POINT('',(0.23094010767585,-0.5,0.));
#6236=CARTESIAN_POINT('',(0.115470053837925,-0.5,-0.2));
#6237=CARTESIAN_POINT('',(0.23094010767585,-0.5,0.));
#6238=CARTESIAN_POINT('',(0.115470053837925,-0.8,-0.2));
#6239=CARTESIAN_POINT('',(0.115470053837925,-0.5,-0.2));
#6240=CARTESIAN_POINT('',(0.23094010767585,-0.8,0.));
#6241=CARTESIAN_POINT('',(0.23094010767585,-0.8,0.));
#6242=CARTESIAN_POINT('',(0.23094010767585,-0.5,0.));
#6243=CARTESIAN_POINT('Origin',(-0.115470053837925,-0.5,-0.2));
#6244=CARTESIAN_POINT('',(-0.115470053837925,-0.5,-0.2));
#6245=CARTESIAN_POINT('',(0.115470053837925,-0.5,-0.2));
#6246=CARTESIAN_POINT('',(-0.115470053837925,-0.8,-0.2));
#6247=CARTESIAN_POINT('',(-0.115470053837925,-0.5,-0.2));
#6248=CARTESIAN_POINT('',(0.115470053837925,-0.8,-0.2));
#6249=CARTESIAN_POINT('Origin',(-0.23094010767585,-0.5,-2.77555756156289E-17));
#6250=CARTESIAN_POINT('',(-0.23094010767585,-0.5,-2.82820063659975E-17));
#6251=CARTESIAN_POINT('',(-0.115470053837925,-0.5,-0.2));
#6252=CARTESIAN_POINT('',(-0.23094010767585,-0.8,-2.77555756156289E-17));
#6253=CARTESIAN_POINT('',(-0.23094010767585,-0.5,-2.82820063659975E-17));
#6254=CARTESIAN_POINT('',(-0.115470053837925,-0.8,-0.2));
#6255=CARTESIAN_POINT('Origin',(-0.115470053837925,-0.5,0.2));
#6256=CARTESIAN_POINT('',(-0.115470053837925,-0.5,0.2));
#6257=CARTESIAN_POINT('',(-0.23094010767585,-0.5,-2.82820063659975E-17));
#6258=CARTESIAN_POINT('',(-0.115470053837925,-0.8,0.2));
#6259=CARTESIAN_POINT('',(-0.115470053837925,-0.5,0.2));
#6260=CARTESIAN_POINT('',(-0.23094010767585,-0.8,-2.82820063659975E-17));
#6261=CARTESIAN_POINT('Origin',(0.115470053837925,-0.5,0.2));
#6262=CARTESIAN_POINT('',(0.115470053837925,-0.5,0.2));
#6263=CARTESIAN_POINT('',(-0.115470053837925,-0.5,0.2));
#6264=CARTESIAN_POINT('',(0.115470053837925,-0.8,0.2));
#6265=CARTESIAN_POINT('',(0.115470053837925,-0.5,0.2));
#6266=CARTESIAN_POINT('',(-0.115470053837925,-0.8,0.2));
#6267=CARTESIAN_POINT('Origin',(0.23094010767585,-0.5,0.));
#6268=CARTESIAN_POINT('',(0.115470053837925,-0.5,0.2));
#6269=CARTESIAN_POINT('',(0.115470053837925,-0.8,0.2));
#6270=CARTESIAN_POINT('Origin',(0.,-0.5,0.));
#6271=CARTESIAN_POINT('Origin',(0.,-0.8,0.));
#6438=UNCERTAINTY_MEASURE_WITH_UNIT(LENGTH_MEASURE(0.001),#6464,
'DISTANCE_ACCURACY_VALUE',
'Maximum model space distance between geometric entities at asserted c
onnectivities');
#6442=UNCERTAINTY_MEASURE_WITH_UNIT(LENGTH_MEASURE(0.001),#6464,
'DISTANCE_ACCURACY_VALUE',
'Maximum model space distance between geometric entities at asserted c
onnectivities');
#6459=(
GEOMETRIC_REPRESENTATION_CONTEXT(3)
GLOBAL_UNCERTAINTY_ASSIGNED_CONTEXT((#6438))
GLOBAL_UNIT_ASSIGNED_CONTEXT((#6464,#6466,#6467))
REPRESENTATION_CONTEXT('','3D')
);
#6463=(
GEOMETRIC_REPRESENTATION_CONTEXT(3)
GLOBAL_UNCERTAINTY_ASSIGNED_CONTEXT((#6442))
GLOBAL_UNIT_ASSIGNED_CONTEXT((#6464,#6466,#6467))
REPRESENTATION_CONTEXT('','3D')
);
#6464=(
LENGTH_UNIT()
NAMED_UNIT(*)
SI_UNIT(.CENTI.,.METRE.)
);
#6466=(
NAMED_UNIT(*)
PLANE_ANGLE_UNIT()
SI_UNIT($,.RADIAN.)
);
#6467=(
NAMED_UNIT(*)
SI_UNIT($,.STERADIAN.)
SOLID_ANGLE_UNIT()
);
#6484=SHAPE_DEFINITION_REPRESENTATION(#6506,#6576);
#6506=PRODUCT_DEFINITION_SHAPE('',$,#6597);
#6576=SHAPE_REPRESENTATION('',(#4147),#6459);
#6580=PRODUCT_DEFINITION_CONTEXT('part definition',#6642,'design');
#6597=PRODUCT_DEFINITION('Cap Screw - M5x20','Cap Screw - M5x20',#6617,
#6580);
#6617=PRODUCT_DEFINITION_FORMATION('',$,#6660);
#6642=APPLICATION_CONTEXT(
'Core Data for Automotive Mechanical Design Process');
#6643=PRODUCT_CONTEXT('part definition',#6642,'mechanical');
#6660=PRODUCT('Cap Screw - M5x20','Cap Screw - M5x20',
'Cap Screw - M5x20',(#6643));
#6741=COLOUR_RGB('Black',0.12,0.14,0.17);
#6742=FILL_AREA_STYLE_COLOUR('',#6741);
#6743=FILL_AREA_STYLE('',(#6742));
#6744=SURFACE_STYLE_FILL_AREA(#6743);
#6745=SURFACE_SIDE_STYLE('',(#6744));
#6746=SURFACE_STYLE_USAGE(.BOTH.,#6745);
#6747=PRESENTATION_STYLE_ASSIGNMENT((#6746));
ENDSEC;
END-ISO-10303-21;
